ISO-10303-21;
HEADER;
/* Generated by software containing ST-Developer
 * from STEP Tools, Inc. (www.steptools.com) 
 */

FILE_DESCRIPTION(
/* description */ ('PAT-091'),
/* implementation_level */ '2;1');

FILE_NAME(
/* name */ 'M4 low-profile retaining screw (4).step',
/* time_stamp */ '2026-10-27T15:34:44-07:00',
/* author */ (''),
/* organization */ (''),
/* preprocessor_version */ 'ST-DEVELOPER v20.2',
/* originating_system */ 'Autodesk Translation Framework v15.17.0.0',
/* authorisation */ '');

FILE_SCHEMA (('AUTOMOTIVE_DESIGN { 1 0 10303 214 3 1 1 }'));
ENDSEC;

DATA;
#10=MECHANICAL_DESIGN_GEOMETRIC_PRESENTATION_REPRESENTATION('',(#1053),#25100);
#833=SHAPE_REPRESENTATION_RELATIONSHIP('SRR','None',#25600,#943);
#943=ADVANCED_BREP_SHAPE_REPRESENTATION('',(#1174),#25070);
#1053=STYLED_ITEM('',(#26198),#1174);
#1174=MANIFOLD_SOLID_BREP('Body1',#13333);
#1567=FACE_BOUND('',#3845,.T.);
#1974=PLANE('',#15913);
#1975=PLANE('',#15918);
#1976=PLANE('',#15921);
#2674=FACE_OUTER_BOUND('',#3844,.T.);
#2675=FACE_OUTER_BOUND('',#3846,.T.);
#2676=FACE_OUTER_BOUND('',#3847,.T.);
#2677=FACE_OUTER_BOUND('',#3848,.T.);
#2678=FACE_OUTER_BOUND('',#3849,.T.);
#3844=EDGE_LOOP('',(#11378));
#3845=EDGE_LOOP('',(#11379));
#3846=EDGE_LOOP('',(#11380,#11381,#11382,#11383));
#3847=EDGE_LOOP('',(#11384));
#3848=EDGE_LOOP('',(#11385,#11386,#11387,#11388));
#3849=EDGE_LOOP('',(#11389));
#4771=LINE('',#23811,#5511);
#4772=LINE('',#23815,#5512);
#5511=VECTOR('',#19781,0.350000000000001);
#5512=VECTOR('',#19786,0.199999999999999);
#6156=CIRCLE('',#15914,0.350000000000001);
#6157=CIRCLE('',#15915,0.199999999999999);
#6158=CIRCLE('',#15917,0.350000000000001);
#6159=CIRCLE('',#15920,0.199999999999999);
#7181=VERTEX_POINT('',#23804);
#7182=VERTEX_POINT('',#23806);
#7183=VERTEX_POINT('',#23809);
#7184=VERTEX_POINT('',#23814);
#8624=EDGE_CURVE('',#7181,#7181,#6156,.T.);
#8625=EDGE_CURVE('',#7182,#7182,#6157,.T.);
#8626=EDGE_CURVE('',#7183,#7183,#6158,.T.);
#8627=EDGE_CURVE('',#7183,#7181,#4771,.T.);
#8628=EDGE_CURVE('',#7182,#7184,#4772,.T.);
#8629=EDGE_CURVE('',#7184,#7184,#6159,.T.);
#11378=ORIENTED_EDGE('',*,*,#8624,.F.);
#11379=ORIENTED_EDGE('',*,*,#8625,.T.);
#11380=ORIENTED_EDGE('',*,*,#8626,.F.);
#11381=ORIENTED_EDGE('',*,*,#8627,.T.);
#11382=ORIENTED_EDGE('',*,*,#8624,.T.);
#11383=ORIENTED_EDGE('',*,*,#8627,.F.);
#11384=ORIENTED_EDGE('',*,*,#8626,.T.);
#11385=ORIENTED_EDGE('',*,*,#8625,.F.);
#11386=ORIENTED_EDGE('',*,*,#8628,.T.);
#11387=ORIENTED_EDGE('',*,*,#8629,.T.);
#11388=ORIENTED_EDGE('',*,*,#8628,.F.);
#11389=ORIENTED_EDGE('',*,*,#8629,.F.);
#12339=CYLINDRICAL_SURFACE('',#15916,0.350000000000001);
#12340=CYLINDRICAL_SURFACE('',#15919,0.199999999999999);
#13041=ADVANCED_FACE('',(#2674,#1567),#1974,.F.);
#13042=ADVANCED_FACE('',(#2675),#12339,.T.);
#13043=ADVANCED_FACE('',(#2676),#1975,.T.);
#13044=ADVANCED_FACE('',(#2677),#12340,.T.);
#13045=ADVANCED_FACE('',(#2678),#1976,.F.);
#13333=CLOSED_SHELL('',(#13041,#13042,#13043,#13044,#13045));
#15912=AXIS2_PLACEMENT_3D('',#23802,#19769,#19770);
#15913=AXIS2_PLACEMENT_3D('',#23803,#19771,#19772);
#15914=AXIS2_PLACEMENT_3D('',#23805,#19773,#19774);
#15915=AXIS2_PLACEMENT_3D('',#23807,#19775,#19776);
#15916=AXIS2_PLACEMENT_3D('',#23808,#19777,#19778);
#15917=AXIS2_PLACEMENT_3D('',#23810,#19779,#19780);
#15918=AXIS2_PLACEMENT_3D('',#23812,#19782,#19783);
#15919=AXIS2_PLACEMENT_3D('',#23813,#19784,#19785);
#15920=AXIS2_PLACEMENT_3D('',#23816,#19787,#19788);
#15921=AXIS2_PLACEMENT_3D('',#23817,#19789,#19790);
#19769=DIRECTION('axis',(0.,0.,1.));
#19770=DIRECTION('refdir',(1.,0.,0.));
#19771=DIRECTION('center_axis',(0.,1.,0.));
#19772=DIRECTION('ref_axis',(1.,0.,0.));
#19773=DIRECTION('center_axis',(0.,1.,0.));
#19774=DIRECTION('ref_axis',(1.,0.,0.));
#19775=DIRECTION('center_axis',(0.,1.,0.));
#19776=DIRECTION('ref_axis',(1.,0.,0.));
#19777=DIRECTION('center_axis',(0.,1.,0.));
#19778=DIRECTION('ref_axis',(1.,0.,0.));
#19779=DIRECTION('center_axis',(0.,1.,0.));
#19780=DIRECTION('ref_axis',(1.,0.,0.));
#19781=DIRECTION('',(0.,-1.,0.));
#19782=DIRECTION('center_axis',(0.,1.,0.));
#19783=DIRECTION('ref_axis',(1.,0.,0.));
#19784=DIRECTION('center_axis',(0.,1.,0.));
#19785=DIRECTION('ref_axis',(1.,0.,0.));
#19786=DIRECTION('',(0.,-1.,0.));
#19787=DIRECTION('center_axis',(0.,1.,0.));
#19788=DIRECTION('ref_axis',(1.,0.,0.));
#19789=DIRECTION('center_axis',(0.,1.,0.));
#19790=DIRECTION('ref_axis',(1.,0.,0.));
#23802=CARTESIAN_POINT('',(0.,0.,0.));
#23803=CARTESIAN_POINT('Origin',(20.6730642762322,-4.2,9.30814754519511));
#23804=CARTESIAN_POINT('',(20.3230642762322,-4.2,9.30814754519511));
#23805=CARTESIAN_POINT('Origin',(20.6730642762322,-4.2,9.30814754519511));
#23806=CARTESIAN_POINT('',(20.4730642762322,-4.2,9.30814754519511));
#23807=CARTESIAN_POINT('Origin',(20.6730642762322,-4.2,9.30814754519511));
#23808=CARTESIAN_POINT('Origin',(20.6730642762322,-4.2,9.30814754519511));
#23809=CARTESIAN_POINT('',(20.3230642762322,-4.1,9.30814754519511));
#23810=CARTESIAN_POINT('Origin',(20.6730642762322,-4.1,9.30814754519511));
#23811=CARTESIAN_POINT('',(20.3230642762322,-4.2,9.30814754519511));
#23812=CARTESIAN_POINT('Origin',(20.6730642762322,-4.1,9.30814754519511));
#23813=CARTESIAN_POINT('Origin',(20.6730642762322,-4.9,9.30814754519511));
#23814=CARTESIAN_POINT('',(20.4730642762322,-4.9,9.30814754519511));
#23815=CARTESIAN_POINT('',(20.4730642762322,-4.9,9.30814754519511));
#23816=CARTESIAN_POINT('Origin',(20.6730642762322,-4.9,9.30814754519511));
#23817=CARTESIAN_POINT('Origin',(20.6730642762322,-4.9,9.30814754519511));
#24949=UNCERTAINTY_MEASURE_WITH_UNIT(LENGTH_MEASURE(0.001),#25101,
'DISTANCE_ACCURACY_VALUE',
'Maximum model space distance between geometric entities at asserted c
onnectivities');
#24979=UNCERTAINTY_MEASURE_WITH_UNIT(LENGTH_MEASURE(0.001),#25101,
'DISTANCE_ACCURACY_VALUE',
'Maximum model space distance between geometric entities at asserted c
onnectivities');
#25070=(
GEOMETRIC_REPRESENTATION_CONTEXT(3)
GLOBAL_UNCERTAINTY_ASSIGNED_CONTEXT((#24949))
GLOBAL_UNIT_ASSIGNED_CONTEXT((#25101,#25103,#25104))
REPRESENTATION_CONTEXT('','3D')
);
#25100=(
GEOMETRIC_REPRESENTATION_CONTEXT(3)
GLOBAL_UNCERTAINTY_ASSIGNED_CONTEXT((#24979))
GLOBAL_UNIT_ASSIGNED_CONTEXT((#25101,#25103,#25104))
REPRESENTATION_CONTEXT('','3D')
);
#25101=(
LENGTH_UNIT()
NAMED_UNIT(*)
SI_UNIT(.CENTI.,.METRE.)
);
#25103=(
NAMED_UNIT(*)
PLANE_ANGLE_UNIT()
SI_UNIT($,.RADIAN.)
);
#25104=(
NAMED_UNIT(*)
SI_UNIT($,.STERADIAN.)
SOLID_ANGLE_UNIT()
);
#25195=SHAPE_DEFINITION_REPRESENTATION(#25389,#25600);
#25389=PRODUCT_DEFINITION_SHAPE('',$,#25721);
#25600=SHAPE_REPRESENTATION('',(#15912),#25070);
#25630=PRODUCT_DEFINITION_CONTEXT('part definition',#25992,'design');
#25721=PRODUCT_DEFINITION('M4 low-profile retaining screw (4)',
'M4 low-profile retaining screw (4)',#25841,#25630);
#25841=PRODUCT_DEFINITION_FORMATION('',$,#26084);
#25992=APPLICATION_CONTEXT(
'Core Data for Automotive Mechanical Design Process');
#25993=PRODUCT_CONTEXT('part definition',#25992,'mechanical');
#26084=PRODUCT('M4 low-profile retaining screw (4)',
'M4 low-profile retaining screw (4)','M4 low-profile retaining screw (4)',(#25993));
#26192=COLOUR_RGB('Black',0.12,0.14,0.17);
#26193=FILL_AREA_STYLE_COLOUR('',#26192);
#26194=FILL_AREA_STYLE('',(#26193));
#26195=SURFACE_STYLE_FILL_AREA(#26194);
#26196=SURFACE_SIDE_STYLE('',(#26195));
#26197=SURFACE_STYLE_USAGE(.BOTH.,#26196);
#26198=PRESENTATION_STYLE_ASSIGNMENT((#26197));
ENDSEC;
END-ISO-10303-21;
